ISO-10303-21;
HEADER;
/* Generated by software containing ST-Developer
 * from STEP Tools, Inc. (www.steptools.com) 
 */

FILE_DESCRIPTION(
/* description */ ('PAT-080'),
/* implementation_level */ '2;1');

FILE_NAME(
/* name */ 'Pipe clamp cap (1).step',
/* time_stamp */ '2026-10-29T20:13:47-07:00',
/* author */ (''),
/* organization */ (''),
/* preprocessor_version */ 'ST-DEVELOPER v20.2',
/* originating_system */ 'Autodesk Translation Framework v15.17.0.0',
/* authorisation */ '');

FILE_SCHEMA (('AUTOMOTIVE_DESIGN { 1 0 10303 214 3 1 1 }'));
ENDSEC;

DATA;
#10=MECHANICAL_DESIGN_GEOMETRIC_PRESENTATION_REPRESENTATION('',(#252),#6878);
#214=SHAPE_REPRESENTATION_RELATIONSHIP('SRR','None',#6970,#233);
#233=ADVANCED_BREP_SHAPE_REPRESENTATION('',(#271),#6865);
#252=STYLED_ITEM('',(#7143),#271);
#271=MANIFOLD_SOLID_BREP('Body1',#3868);
#305=FACE_BOUND('',#831,.T.);
#306=FACE_BOUND('',#834,.T.);
#307=FACE_BOUND('',#843,.T.);
#308=FACE_BOUND('',#847,.T.);
#418=PLANE('',#4220);
#419=PLANE('',#4225);
#420=PLANE('',#4230);
#421=PLANE('',#4231);
#422=PLANE('',#4239);
#423=PLANE('',#4240);
#424=PLANE('',#4241);
#425=PLANE('',#4242);
#426=PLANE('',#4243);
#580=FACE_OUTER_BOUND('',#830,.T.);
#581=FACE_OUTER_BOUND('',#832,.T.);
#582=FACE_OUTER_BOUND('',#833,.T.);
#583=FACE_OUTER_BOUND('',#835,.T.);
#584=FACE_OUTER_BOUND('',#836,.T.);
#585=FACE_OUTER_BOUND('',#837,.T.);
#586=FACE_OUTER_BOUND('',#838,.T.);
#587=FACE_OUTER_BOUND('',#839,.T.);
#588=FACE_OUTER_BOUND('',#840,.T.);
#589=FACE_OUTER_BOUND('',#841,.T.);
#590=FACE_OUTER_BOUND('',#842,.T.);
#591=FACE_OUTER_BOUND('',#844,.T.);
#592=FACE_OUTER_BOUND('',#845,.T.);
#593=FACE_OUTER_BOUND('',#846,.T.);
#830=EDGE_LOOP('',(#2992,#2993));
#831=EDGE_LOOP('',(#2994));
#832=EDGE_LOOP('',(#2995,#2996,#2997,#2998));
#833=EDGE_LOOP('',(#2999,#3000));
#834=EDGE_LOOP('',(#3001));
#835=EDGE_LOOP('',(#3002,#3003,#3004,#3005));
#836=EDGE_LOOP('',(#3006,#3007,#3008,#3009,#3010,#3011,#3012,#3013));
#837=EDGE_LOOP('',(#3014,#3015,#3016,#3017,#3018,#3019,#3020,#3021));
#838=EDGE_LOOP('',(#3022,#3023,#3024,#3025));
#839=EDGE_LOOP('',(#3026,#3027,#3028,#3029));
#840=EDGE_LOOP('',(#3030,#3031,#3032,#3033));
#841=EDGE_LOOP('',(#3034,#3035,#3036,#3037,#3038,#3039));
#842=EDGE_LOOP('',(#3040,#3041,#3042,#3043));
#843=EDGE_LOOP('',(#3044));
#844=EDGE_LOOP('',(#3045,#3046,#3047,#3048,#3049,#3050));
#845=EDGE_LOOP('',(#3051,#3052,#3053,#3054,#3055,#3056,#3057,#3058));
#846=EDGE_LOOP('',(#3059,#3060,#3061,#3062));
#847=EDGE_LOOP('',(#3063));
#1182=LINE('',#6140,#1497);
#1183=LINE('',#6146,#1498);
#1184=LINE('',#6149,#1499);
#1185=LINE('',#6153,#1500);
#1186=LINE('',#6159,#1501);
#1187=LINE('',#6162,#1502);
#1188=LINE('',#6165,#1503);
#1189=LINE('',#6167,#1504);
#1190=LINE('',#6169,#1505);
#1191=LINE('',#6171,#1506);
#1192=LINE('',#6172,#1507);
#1193=LINE('',#6175,#1508);
#1194=LINE('',#6177,#1509);
#1195=LINE('',#6179,#1510);
#1196=LINE('',#6181,#1511);
#1197=LINE('',#6182,#1512);
#1198=LINE('',#6186,#1513);
#1199=LINE('',#6190,#1514);
#1200=LINE('',#6196,#1515);
#1201=LINE('',#6199,#1516);
#1202=LINE('',#6201,#1517);
#1203=LINE('',#6202,#1518);
#1204=LINE('',#6203,#1519);
#1205=LINE('',#6205,#1520);
#1206=LINE('',#6207,#1521);
#1207=LINE('',#6208,#1522);
#1497=VECTOR('',#4942,1.);
#1498=VECTOR('',#4949,1.);
#1499=VECTOR('',#4952,1.);
#1500=VECTOR('',#4955,1.);
#1501=VECTOR('',#4962,1.);
#1502=VECTOR('',#4965,1.);
#1503=VECTOR('',#4968,1.);
#1504=VECTOR('',#4969,1.);
#1505=VECTOR('',#4970,1.);
#1506=VECTOR('',#4971,1.);
#1507=VECTOR('',#4972,1.);
#1508=VECTOR('',#4975,1.);
#1509=VECTOR('',#4976,1.);
#1510=VECTOR('',#4977,1.);
#1511=VECTOR('',#4978,1.);
#1512=VECTOR('',#4979,1.);
#1513=VECTOR('',#4984,0.275);
#1514=VECTOR('',#4989,0.275);
#1515=VECTOR('',#4994,1.);
#1516=VECTOR('',#4997,1.);
#1517=VECTOR('',#5000,1.);
#1518=VECTOR('',#5001,1.);
#1519=VECTOR('',#5002,1.);
#1520=VECTOR('',#5005,1.);
#1521=VECTOR('',#5008,1.);
#1522=VECTOR('',#5009,1.);
#1696=CIRCLE('',#4221,0.475);
#1697=CIRCLE('',#4222,0.275);
#1698=CIRCLE('',#4224,0.475);
#1699=CIRCLE('',#4226,0.475);
#1700=CIRCLE('',#4227,0.275);
#1701=CIRCLE('',#4229,0.475);
#1702=CIRCLE('',#4233,0.275);
#1703=CIRCLE('',#4235,0.275);
#1704=CIRCLE('',#4237,1.31);
#1705=CIRCLE('',#4238,1.31);
#1938=VERTEX_POINT('',#6138);
#1939=VERTEX_POINT('',#6139);
#1940=VERTEX_POINT('',#6142);
#1941=VERTEX_POINT('',#6145);
#1942=VERTEX_POINT('',#6147);
#1943=VERTEX_POINT('',#6151);
#1944=VERTEX_POINT('',#6152);
#1945=VERTEX_POINT('',#6155);
#1946=VERTEX_POINT('',#6158);
#1947=VERTEX_POINT('',#6160);
#1948=VERTEX_POINT('',#6164);
#1949=VERTEX_POINT('',#6166);
#1950=VERTEX_POINT('',#6168);
#1951=VERTEX_POINT('',#6170);
#1952=VERTEX_POINT('',#6174);
#1953=VERTEX_POINT('',#6176);
#1954=VERTEX_POINT('',#6178);
#1955=VERTEX_POINT('',#6180);
#1956=VERTEX_POINT('',#6184);
#1957=VERTEX_POINT('',#6188);
#1958=VERTEX_POINT('',#6192);
#1959=VERTEX_POINT('',#6193);
#1960=VERTEX_POINT('',#6195);
#1961=VERTEX_POINT('',#6197);
#2319=EDGE_CURVE('',#1938,#1939,#1182,.T.);
#2320=EDGE_CURVE('',#1938,#1939,#1696,.T.);
#2321=EDGE_CURVE('',#1940,#1940,#1697,.T.);
#2322=EDGE_CURVE('',#1941,#1938,#1183,.T.);
#2323=EDGE_CURVE('',#1942,#1941,#1698,.T.);
#2324=EDGE_CURVE('',#1939,#1942,#1184,.T.);
#2325=EDGE_CURVE('',#1943,#1944,#1185,.T.);
#2326=EDGE_CURVE('',#1943,#1944,#1699,.T.);
#2327=EDGE_CURVE('',#1945,#1945,#1700,.T.);
#2328=EDGE_CURVE('',#1946,#1943,#1186,.T.);
#2329=EDGE_CURVE('',#1947,#1946,#1701,.T.);
#2330=EDGE_CURVE('',#1944,#1947,#1187,.T.);
#2331=EDGE_CURVE('',#1948,#1942,#1188,.T.);
#2332=EDGE_CURVE('',#1949,#1948,#1189,.T.);
#2333=EDGE_CURVE('',#1949,#1950,#1190,.T.);
#2334=EDGE_CURVE('',#1950,#1951,#1191,.T.);
#2335=EDGE_CURVE('',#1941,#1951,#1192,.T.);
#2336=EDGE_CURVE('',#1952,#1947,#1193,.T.);
#2337=EDGE_CURVE('',#1953,#1952,#1194,.T.);
#2338=EDGE_CURVE('',#1953,#1954,#1195,.T.);
#2339=EDGE_CURVE('',#1954,#1955,#1196,.T.);
#2340=EDGE_CURVE('',#1946,#1955,#1197,.T.);
#2341=EDGE_CURVE('',#1956,#1956,#1702,.T.);
#2342=EDGE_CURVE('',#1956,#1940,#1198,.T.);
#2343=EDGE_CURVE('',#1957,#1957,#1703,.T.);
#2344=EDGE_CURVE('',#1957,#1945,#1199,.T.);
#2345=EDGE_CURVE('',#1958,#1959,#1704,.T.);
#2346=EDGE_CURVE('',#1960,#1958,#1200,.T.);
#2347=EDGE_CURVE('',#1961,#1960,#1705,.T.);
#2348=EDGE_CURVE('',#1959,#1961,#1201,.T.);
#2349=EDGE_CURVE('',#1960,#1953,#1202,.T.);
#2350=EDGE_CURVE('',#1951,#1952,#1203,.T.);
#2351=EDGE_CURVE('',#1950,#1961,#1204,.T.);
#2352=EDGE_CURVE('',#1954,#1958,#1205,.T.);
#2353=EDGE_CURVE('',#1959,#1949,#1206,.T.);
#2354=EDGE_CURVE('',#1955,#1948,#1207,.T.);
#2992=ORIENTED_EDGE('',*,*,#2319,.F.);
#2993=ORIENTED_EDGE('',*,*,#2320,.T.);
#2994=ORIENTED_EDGE('',*,*,#2321,.F.);
#2995=ORIENTED_EDGE('',*,*,#2322,.F.);
#2996=ORIENTED_EDGE('',*,*,#2323,.F.);
#2997=ORIENTED_EDGE('',*,*,#2324,.F.);
#2998=ORIENTED_EDGE('',*,*,#2320,.F.);
#2999=ORIENTED_EDGE('',*,*,#2325,.F.);
#3000=ORIENTED_EDGE('',*,*,#2326,.T.);
#3001=ORIENTED_EDGE('',*,*,#2327,.F.);
#3002=ORIENTED_EDGE('',*,*,#2328,.F.);
#3003=ORIENTED_EDGE('',*,*,#2329,.F.);
#3004=ORIENTED_EDGE('',*,*,#2330,.F.);
#3005=ORIENTED_EDGE('',*,*,#2326,.F.);
#3006=ORIENTED_EDGE('',*,*,#2322,.T.);
#3007=ORIENTED_EDGE('',*,*,#2319,.T.);
#3008=ORIENTED_EDGE('',*,*,#2324,.T.);
#3009=ORIENTED_EDGE('',*,*,#2331,.F.);
#3010=ORIENTED_EDGE('',*,*,#2332,.F.);
#3011=ORIENTED_EDGE('',*,*,#2333,.T.);
#3012=ORIENTED_EDGE('',*,*,#2334,.T.);
#3013=ORIENTED_EDGE('',*,*,#2335,.F.);
#3014=ORIENTED_EDGE('',*,*,#2328,.T.);
#3015=ORIENTED_EDGE('',*,*,#2325,.T.);
#3016=ORIENTED_EDGE('',*,*,#2330,.T.);
#3017=ORIENTED_EDGE('',*,*,#2336,.F.);
#3018=ORIENTED_EDGE('',*,*,#2337,.F.);
#3019=ORIENTED_EDGE('',*,*,#2338,.T.);
#3020=ORIENTED_EDGE('',*,*,#2339,.T.);
#3021=ORIENTED_EDGE('',*,*,#2340,.F.);
#3022=ORIENTED_EDGE('',*,*,#2341,.F.);
#3023=ORIENTED_EDGE('',*,*,#2342,.T.);
#3024=ORIENTED_EDGE('',*,*,#2321,.T.);
#3025=ORIENTED_EDGE('',*,*,#2342,.F.);
#3026=ORIENTED_EDGE('',*,*,#2343,.F.);
#3027=ORIENTED_EDGE('',*,*,#2344,.T.);
#3028=ORIENTED_EDGE('',*,*,#2327,.T.);
#3029=ORIENTED_EDGE('',*,*,#2344,.F.);
#3030=ORIENTED_EDGE('',*,*,#2345,.F.);
#3031=ORIENTED_EDGE('',*,*,#2346,.F.);
#3032=ORIENTED_EDGE('',*,*,#2347,.F.);
#3033=ORIENTED_EDGE('',*,*,#2348,.F.);
#3034=ORIENTED_EDGE('',*,*,#2347,.T.);
#3035=ORIENTED_EDGE('',*,*,#2349,.T.);
#3036=ORIENTED_EDGE('',*,*,#2337,.T.);
#3037=ORIENTED_EDGE('',*,*,#2350,.F.);
#3038=ORIENTED_EDGE('',*,*,#2334,.F.);
#3039=ORIENTED_EDGE('',*,*,#2351,.T.);
#3040=ORIENTED_EDGE('',*,*,#2346,.T.);
#3041=ORIENTED_EDGE('',*,*,#2352,.F.);
#3042=ORIENTED_EDGE('',*,*,#2338,.F.);
#3043=ORIENTED_EDGE('',*,*,#2349,.F.);
#3044=ORIENTED_EDGE('',*,*,#2343,.T.);
#3045=ORIENTED_EDGE('',*,*,#2345,.T.);
#3046=ORIENTED_EDGE('',*,*,#2353,.T.);
#3047=ORIENTED_EDGE('',*,*,#2332,.T.);
#3048=ORIENTED_EDGE('',*,*,#2354,.F.);
#3049=ORIENTED_EDGE('',*,*,#2339,.F.);
#3050=ORIENTED_EDGE('',*,*,#2352,.T.);
#3051=ORIENTED_EDGE('',*,*,#2323,.T.);
#3052=ORIENTED_EDGE('',*,*,#2335,.T.);
#3053=ORIENTED_EDGE('',*,*,#2350,.T.);
#3054=ORIENTED_EDGE('',*,*,#2336,.T.);
#3055=ORIENTED_EDGE('',*,*,#2329,.T.);
#3056=ORIENTED_EDGE('',*,*,#2340,.T.);
#3057=ORIENTED_EDGE('',*,*,#2354,.T.);
#3058=ORIENTED_EDGE('',*,*,#2331,.T.);
#3059=ORIENTED_EDGE('',*,*,#2348,.T.);
#3060=ORIENTED_EDGE('',*,*,#2351,.F.);
#3061=ORIENTED_EDGE('',*,*,#2333,.F.);
#3062=ORIENTED_EDGE('',*,*,#2353,.F.);
#3063=ORIENTED_EDGE('',*,*,#2341,.T.);
#3589=CYLINDRICAL_SURFACE('',#4223,0.475);
#3590=CYLINDRICAL_SURFACE('',#4228,0.475);
#3591=CYLINDRICAL_SURFACE('',#4232,0.275);
#3592=CYLINDRICAL_SURFACE('',#4234,0.275);
#3593=CYLINDRICAL_SURFACE('',#4236,1.31);
#3716=ADVANCED_FACE('',(#580,#305),#418,.T.);
#3717=ADVANCED_FACE('',(#581),#3589,.F.);
#3718=ADVANCED_FACE('',(#582,#306),#419,.T.);
#3719=ADVANCED_FACE('',(#583),#3590,.F.);
#3720=ADVANCED_FACE('',(#584),#420,.T.);
#3721=ADVANCED_FACE('',(#585),#421,.T.);
#3722=ADVANCED_FACE('',(#586),#3591,.F.);
#3723=ADVANCED_FACE('',(#587),#3592,.F.);
#3724=ADVANCED_FACE('',(#588),#3593,.F.);
#3725=ADVANCED_FACE('',(#589),#422,.T.);
#3726=ADVANCED_FACE('',(#590,#307),#423,.F.);
#3727=ADVANCED_FACE('',(#591),#424,.T.);
#3728=ADVANCED_FACE('',(#592),#425,.T.);
#3729=ADVANCED_FACE('',(#593,#308),#426,.F.);
#3868=CLOSED_SHELL('',(#3716,#3717,#3718,#3719,#3720,#3721,#3722,#3723,
#3724,#3725,#3726,#3727,#3728,#3729));
#4219=AXIS2_PLACEMENT_3D('',#6136,#4938,#4939);
#4220=AXIS2_PLACEMENT_3D('',#6137,#4940,#4941);
#4221=AXIS2_PLACEMENT_3D('',#6141,#4943,#4944);
#4222=AXIS2_PLACEMENT_3D('',#6143,#4945,#4946);
#4223=AXIS2_PLACEMENT_3D('',#6144,#4947,#4948);
#4224=AXIS2_PLACEMENT_3D('',#6148,#4950,#4951);
#4225=AXIS2_PLACEMENT_3D('',#6150,#4953,#4954);
#4226=AXIS2_PLACEMENT_3D('',#6154,#4956,#4957);
#4227=AXIS2_PLACEMENT_3D('',#6156,#4958,#4959);
#4228=AXIS2_PLACEMENT_3D('',#6157,#4960,#4961);
#4229=AXIS2_PLACEMENT_3D('',#6161,#4963,#4964);
#4230=AXIS2_PLACEMENT_3D('',#6163,#4966,#4967);
#4231=AXIS2_PLACEMENT_3D('',#6173,#4973,#4974);
#4232=AXIS2_PLACEMENT_3D('',#6183,#4980,#4981);
#4233=AXIS2_PLACEMENT_3D('',#6185,#4982,#4983);
#4234=AXIS2_PLACEMENT_3D('',#6187,#4985,#4986);
#4235=AXIS2_PLACEMENT_3D('',#6189,#4987,#4988);
#4236=AXIS2_PLACEMENT_3D('',#6191,#4990,#4991);
#4237=AXIS2_PLACEMENT_3D('',#6194,#4992,#4993);
#4238=AXIS2_PLACEMENT_3D('',#6198,#4995,#4996);
#4239=AXIS2_PLACEMENT_3D('',#6200,#4998,#4999);
#4240=AXIS2_PLACEMENT_3D('',#6204,#5003,#5004);
#4241=AXIS2_PLACEMENT_3D('',#6206,#5006,#5007);
#4242=AXIS2_PLACEMENT_3D('',#6209,#5010,#5011);
#4243=AXIS2_PLACEMENT_3D('',#6210,#5012,#5013);
#4938=DIRECTION('axis',(0.,0.,1.));
#4939=DIRECTION('refdir',(1.,0.,0.));
#4940=DIRECTION('center_axis',(0.,0.,1.));
#4941=DIRECTION('ref_axis',(1.,0.,0.));
#4942=DIRECTION('',(-1.,0.,0.));
#4943=DIRECTION('center_axis',(0.,0.,1.));
#4944=DIRECTION('ref_axis',(1.,0.,0.));
#4945=DIRECTION('center_axis',(0.,0.,1.));
#4946=DIRECTION('ref_axis',(1.,0.,0.));
#4947=DIRECTION('center_axis',(0.,0.,1.));
#4948=DIRECTION('ref_axis',(6.12323399573677E-17,1.,0.));
#4949=DIRECTION('',(0.,0.,-1.));
#4950=DIRECTION('center_axis',(0.,0.,-1.));
#4951=DIRECTION('ref_axis',(1.,0.,0.));
#4952=DIRECTION('',(0.,0.,1.));
#4953=DIRECTION('center_axis',(0.,0.,1.));
#4954=DIRECTION('ref_axis',(1.,0.,0.));
#4955=DIRECTION('',(1.,0.,0.));
#4956=DIRECTION('center_axis',(0.,0.,1.));
#4957=DIRECTION('ref_axis',(1.,0.,0.));
#4958=DIRECTION('center_axis',(0.,0.,1.));
#4959=DIRECTION('ref_axis',(1.,0.,0.));
#4960=DIRECTION('center_axis',(0.,0.,1.));
#4961=DIRECTION('ref_axis',(-1.83697019872103E-16,-1.,0.));
#4962=DIRECTION('',(0.,0.,-1.));
#4963=DIRECTION('center_axis',(0.,0.,-1.));
#4964=DIRECTION('ref_axis',(1.,0.,0.));
#4965=DIRECTION('',(0.,0.,1.));
#4966=DIRECTION('center_axis',(0.,-1.,0.));
#4967=DIRECTION('ref_axis',(1.,0.,0.));
#4968=DIRECTION('',(1.,0.,0.));
#4969=DIRECTION('',(0.,0.,1.));
#4970=DIRECTION('',(1.,0.,0.));
#4971=DIRECTION('',(0.,0.,1.));
#4972=DIRECTION('',(1.,0.,0.));
#4973=DIRECTION('center_axis',(0.,1.,0.));
#4974=DIRECTION('ref_axis',(-1.,0.,0.));
#4975=DIRECTION('',(-1.,0.,0.));
#4976=DIRECTION('',(0.,0.,1.));
#4977=DIRECTION('',(-1.,0.,0.));
#4978=DIRECTION('',(0.,0.,1.));
#4979=DIRECTION('',(-1.,0.,0.));
#4980=DIRECTION('center_axis',(0.,0.,1.));
#4981=DIRECTION('ref_axis',(1.,0.,0.));
#4982=DIRECTION('center_axis',(0.,0.,1.));
#4983=DIRECTION('ref_axis',(1.,0.,0.));
#4984=DIRECTION('',(0.,0.,1.));
#4985=DIRECTION('center_axis',(0.,0.,1.));
#4986=DIRECTION('ref_axis',(1.,0.,0.));
#4987=DIRECTION('center_axis',(0.,0.,1.));
#4988=DIRECTION('ref_axis',(1.,0.,0.));
#4989=DIRECTION('',(0.,0.,1.));
#4990=DIRECTION('center_axis',(1.,0.,0.));
#4991=DIRECTION('ref_axis',(0.,1.22464679914735E-16,1.));
#4992=DIRECTION('center_axis',(1.,0.,0.));
#4993=DIRECTION('ref_axis',(0.,0.,-1.));
#4994=DIRECTION('',(-1.,0.,0.));
#4995=DIRECTION('center_axis',(-1.,0.,0.));
#4996=DIRECTION('ref_axis',(0.,0.,-1.));
#4997=DIRECTION('',(1.,0.,0.));
#4998=DIRECTION('center_axis',(1.,0.,0.));
#4999=DIRECTION('ref_axis',(0.,1.,0.));
#5000=DIRECTION('',(0.,1.,0.));
#5001=DIRECTION('',(0.,1.,0.));
#5002=DIRECTION('',(0.,1.,0.));
#5003=DIRECTION('center_axis',(0.,0.,1.));
#5004=DIRECTION('ref_axis',(1.,0.,0.));
#5005=DIRECTION('',(0.,-1.,0.));
#5006=DIRECTION('center_axis',(-1.,0.,0.));
#5007=DIRECTION('ref_axis',(0.,-1.,0.));
#5008=DIRECTION('',(0.,-1.,0.));
#5009=DIRECTION('',(0.,-1.,0.));
#5010=DIRECTION('center_axis',(0.,0.,1.));
#5011=DIRECTION('ref_axis',(1.,0.,0.));
#5012=DIRECTION('center_axis',(0.,0.,1.));
#5013=DIRECTION('ref_axis',(1.,0.,0.));
#6136=CARTESIAN_POINT('',(0.,0.,0.));
#6137=CARTESIAN_POINT('Origin',(4.5,-2.,7.));
#6138=CARTESIAN_POINT('',(4.75617376914899,-2.4,7.));
#6139=CARTESIAN_POINT('',(4.24382623085101,-2.4,7.));
#6140=CARTESIAN_POINT('',(4.2,-2.4,7.));
#6141=CARTESIAN_POINT('Origin',(4.5,-2.,7.));
#6142=CARTESIAN_POINT('',(4.225,-2.,7.));
#6143=CARTESIAN_POINT('Origin',(4.5,-2.,7.));
#6144=CARTESIAN_POINT('Origin',(4.5,-2.,7.));
#6145=CARTESIAN_POINT('',(4.75617376914899,-2.4,7.8));
#6146=CARTESIAN_POINT('',(4.75617376914899,-2.4,7.));
#6147=CARTESIAN_POINT('',(4.24382623085101,-2.4,7.8));
#6148=CARTESIAN_POINT('Origin',(4.5,-2.,7.8));
#6149=CARTESIAN_POINT('',(4.24382623085101,-2.4,7.));
#6150=CARTESIAN_POINT('Origin',(4.5,2.,7.));
#6151=CARTESIAN_POINT('',(4.24382623085101,2.4,7.));
#6152=CARTESIAN_POINT('',(4.75617376914899,2.4,7.));
#6153=CARTESIAN_POINT('',(4.8,2.4,7.));
#6154=CARTESIAN_POINT('Origin',(4.5,2.,7.));
#6155=CARTESIAN_POINT('',(4.225,2.,7.));
#6156=CARTESIAN_POINT('Origin',(4.5,2.,7.));
#6157=CARTESIAN_POINT('Origin',(4.5,2.,7.));
#6158=CARTESIAN_POINT('',(4.24382623085101,2.4,7.8));
#6159=CARTESIAN_POINT('',(4.24382623085101,2.4,7.));
#6160=CARTESIAN_POINT('',(4.75617376914899,2.4,7.8));
#6161=CARTESIAN_POINT('Origin',(4.5,2.,7.8));
#6162=CARTESIAN_POINT('',(4.75617376914899,2.4,7.));
#6163=CARTESIAN_POINT('Origin',(3.9,-2.4,6.));
#6164=CARTESIAN_POINT('',(3.9,-2.4,7.8));
#6165=CARTESIAN_POINT('',(3.9,-2.4,7.8));
#6166=CARTESIAN_POINT('',(3.9,-2.4,6.));
#6167=CARTESIAN_POINT('',(3.9,-2.4,6.));
#6168=CARTESIAN_POINT('',(5.1,-2.4,6.));
#6169=CARTESIAN_POINT('',(3.9,-2.4,6.));
#6170=CARTESIAN_POINT('',(5.1,-2.4,7.8));
#6171=CARTESIAN_POINT('',(5.1,-2.4,6.));
#6172=CARTESIAN_POINT('',(3.9,-2.4,7.8));
#6173=CARTESIAN_POINT('Origin',(5.1,2.4,6.));
#6174=CARTESIAN_POINT('',(5.1,2.4,7.8));
#6175=CARTESIAN_POINT('',(5.1,2.4,7.8));
#6176=CARTESIAN_POINT('',(5.1,2.4,6.));
#6177=CARTESIAN_POINT('',(5.1,2.4,6.));
#6178=CARTESIAN_POINT('',(3.9,2.4,6.));
#6179=CARTESIAN_POINT('',(5.1,2.4,6.));
#6180=CARTESIAN_POINT('',(3.9,2.4,7.8));
#6181=CARTESIAN_POINT('',(3.9,2.4,6.));
#6182=CARTESIAN_POINT('',(5.1,2.4,7.8));
#6183=CARTESIAN_POINT('Origin',(4.5,-2.,5.9));
#6184=CARTESIAN_POINT('',(4.225,-2.,6.));
#6185=CARTESIAN_POINT('Origin',(4.5,-2.,6.));
#6186=CARTESIAN_POINT('',(4.225,-2.,5.9));
#6187=CARTESIAN_POINT('Origin',(4.5,2.,5.9));
#6188=CARTESIAN_POINT('',(4.225,2.,6.));
#6189=CARTESIAN_POINT('Origin',(4.5,2.,6.));
#6190=CARTESIAN_POINT('',(4.225,2.,5.9));
#6191=CARTESIAN_POINT('Origin',(3.8,0.,6.));
#6192=CARTESIAN_POINT('',(3.9,1.31,6.));
#6193=CARTESIAN_POINT('',(3.9,-1.31,6.));
#6194=CARTESIAN_POINT('Origin',(3.9,0.,6.));
#6195=CARTESIAN_POINT('',(5.1,1.31,6.));
#6196=CARTESIAN_POINT('',(3.8,1.31,6.));
#6197=CARTESIAN_POINT('',(5.1,-1.31,6.));
#6198=CARTESIAN_POINT('Origin',(5.1,0.,6.));
#6199=CARTESIAN_POINT('',(3.8,-1.31,6.));
#6200=CARTESIAN_POINT('Origin',(5.1,-2.4,6.));
#6201=CARTESIAN_POINT('',(5.1,-2.4,6.));
#6202=CARTESIAN_POINT('',(5.1,-2.4,7.8));
#6203=CARTESIAN_POINT('',(5.1,-2.4,6.));
#6204=CARTESIAN_POINT('Origin',(4.5,0.,6.));
#6205=CARTESIAN_POINT('',(3.9,2.4,6.));
#6206=CARTESIAN_POINT('Origin',(3.9,2.4,6.));
#6207=CARTESIAN_POINT('',(3.9,2.4,6.));
#6208=CARTESIAN_POINT('',(3.9,2.4,7.8));
#6209=CARTESIAN_POINT('Origin',(4.5,0.,7.8));
#6210=CARTESIAN_POINT('Origin',(4.5,0.,6.));
#6844=UNCERTAINTY_MEASURE_WITH_UNIT(LENGTH_MEASURE(0.001),#6879,
'DISTANCE_ACCURACY_VALUE',
'Maximum model space distance between geometric entities at asserted c
onnectivities');
#6857=UNCERTAINTY_MEASURE_WITH_UNIT(LENGTH_MEASURE(0.001),#6879,
'DISTANCE_ACCURACY_VALUE',
'Maximum model space distance between geometric entities at asserted c
onnectivities');
#6865=(
GEOMETRIC_REPRESENTATION_CONTEXT(3)
GLOBAL_UNCERTAINTY_ASSIGNED_CONTEXT((#6844))
GLOBAL_UNIT_ASSIGNED_CONTEXT((#6879,#6881,#6882))
REPRESENTATION_CONTEXT('','3D')
);
#6878=(
GEOMETRIC_REPRESENTATION_CONTEXT(3)
GLOBAL_UNCERTAINTY_ASSIGNED_CONTEXT((#6857))
GLOBAL_UNIT_ASSIGNED_CONTEXT((#6879,#6881,#6882))
REPRESENTATION_CONTEXT('','3D')
);
#6879=(
LENGTH_UNIT()
NAMED_UNIT(*)
SI_UNIT(.CENTI.,.METRE.)
);
#6881=(
NAMED_UNIT(*)
PLANE_ANGLE_UNIT()
SI_UNIT($,.RADIAN.)
);
#6882=(
NAMED_UNIT(*)
SI_UNIT($,.STERADIAN.)
SOLID_ANGLE_UNIT()
);
#6890=SHAPE_DEFINITION_REPRESENTATION(#6910,#6970);
#6910=PRODUCT_DEFINITION_SHAPE('',$,#6991);
#6970=SHAPE_REPRESENTATION('',(#4219),#6865);
#6983=PRODUCT_DEFINITION_CONTEXT('part definition',#7045,'design');
#6991=PRODUCT_DEFINITION('Pipe clamp cap (1)',
'Pipe clamp cap (1)',#7011,#6983);
#7011=PRODUCT_DEFINITION_FORMATION('',$,#7054);
#7045=APPLICATION_CONTEXT(
'Core Data for Automotive Mechanical Design Process');
#7046=PRODUCT_CONTEXT('part definition',#7045,'mechanical');
#7054=PRODUCT('Pipe clamp cap (1)','Pipe clamp cap (1)',
'Pipe clamp cap (1)',(#7046));
#7137=COLOUR_RGB('Off White',0.89,0.88,0.83);
#7138=FILL_AREA_STYLE_COLOUR('',#7137);
#7139=FILL_AREA_STYLE('',(#7138));
#7140=SURFACE_STYLE_FILL_AREA(#7139);
#7141=SURFACE_SIDE_STYLE('',(#7140));
#7142=SURFACE_STYLE_USAGE(.BOTH.,#7141);
#7143=PRESENTATION_STYLE_ASSIGNMENT((#7142));
ENDSEC;
END-ISO-10303-21;
